ISO-10303-21;
HEADER;
/* Generated by software containing ST-Developer
 * from STEP Tools, Inc. (www.steptools.com) 
 */

FILE_DESCRIPTION(
/* description */ ('Located fixture plate with toggle clamp'),
/* implementation_level */ '2;1');

FILE_NAME(
/* name */ 'M8x25 Bolt.step',
/* time_stamp */ '2026-10-27T21:36:12-07:00',
/* author */ (''),
/* organization */ (''),
/* preprocessor_version */ 'ST-DEVELOPER v20.2',
/* originating_system */ 'Autodesk Translation Framework v15.17.0.0',
/* authorisation */ '');

FILE_SCHEMA (('AUTOMOTIVE_DESIGN { 1 0 10303 214 3 1 1 }'));
ENDSEC;

DATA;
#10=MECHANICAL_DESIGN_GEOMETRIC_PRESENTATION_REPRESENTATION('',(#332),#9285);
#245=ORIENTED_CLOSED_SHELL('',*,#5181,.F.);
#248=BREP_WITH_VOIDS('Body1',#5182,(#245));
#261=CONICAL_SURFACE('',#5767,0.625,0.785398163397448);
#262=CONICAL_SURFACE('',#5771,0.635,0.785398163397449);
#263=CONICAL_SURFACE('',#5775,0.41,0.463647609000806);
#284=SHAPE_REPRESENTATION_RELATIONSHIP('SRR','None',#9407,#308);
#308=ADVANCED_BREP_SHAPE_REPRESENTATION('',(#248),#9269);
#332=STYLED_ITEM('',(#9619),#248);
#452=FACE_BOUND('',#1229,.T.);
#583=PLANE('',#5755);
#584=PLANE('',#5756);
#585=PLANE('',#5757);
#586=PLANE('',#5758);
#587=PLANE('',#5759);
#588=PLANE('',#5760);
#589=PLANE('',#5761);
#590=PLANE('',#5762);
#591=PLANE('',#5763);
#592=PLANE('',#5765);
#593=PLANE('',#5773);
#834=FACE_OUTER_BOUND('',#1215,.T.);
#835=FACE_OUTER_BOUND('',#1216,.T.);
#836=FACE_OUTER_BOUND('',#1217,.T.);
#837=FACE_OUTER_BOUND('',#1218,.T.);
#838=FACE_OUTER_BOUND('',#1219,.T.);
#839=FACE_OUTER_BOUND('',#1220,.T.);
#840=FACE_OUTER_BOUND('',#1221,.T.);
#841=FACE_OUTER_BOUND('',#1222,.T.);
#842=FACE_OUTER_BOUND('',#1223,.T.);
#843=FACE_OUTER_BOUND('',#1224,.T.);
#844=FACE_OUTER_BOUND('',#1225,.T.);
#845=FACE_OUTER_BOUND('',#1226,.T.);
#846=FACE_OUTER_BOUND('',#1227,.T.);
#847=FACE_OUTER_BOUND('',#1228,.T.);
#848=FACE_OUTER_BOUND('',#1230,.T.);
#849=FACE_OUTER_BOUND('',#1231,.T.);
#1215=EDGE_LOOP('',(#4240,#4241,#4242,#4243));
#1216=EDGE_LOOP('',(#4244,#4245,#4246,#4247));
#1217=EDGE_LOOP('',(#4248,#4249,#4250,#4251));
#1218=EDGE_LOOP('',(#4252,#4253,#4254,#4255));
#1219=EDGE_LOOP('',(#4256,#4257,#4258,#4259));
#1220=EDGE_LOOP('',(#4260,#4261,#4262,#4263));
#1221=EDGE_LOOP('',(#4264,#4265,#4266,#4267,#4268,#4269));
#1222=EDGE_LOOP('',(#4270,#4271,#4272,#4273,#4274,#4275));
#1223=EDGE_LOOP('',(#4276));
#1224=EDGE_LOOP('',(#4277));
#1225=EDGE_LOOP('',(#4278,#4279,#4280,#4281));
#1226=EDGE_LOOP('',(#4282,#4283,#4284,#4285));
#1227=EDGE_LOOP('',(#4286,#4287,#4288,#4289));
#1228=EDGE_LOOP('',(#4290));
#1229=EDGE_LOOP('',(#4291));
#1230=EDGE_LOOP('',(#4292,#4293,#4294,#4295));
#1231=EDGE_LOOP('',(#4296,#4297,#4298,#4299));
#1502=CIRCLE('',#5764,0.3933);
#1503=CIRCLE('',#5766,0.6);
#1504=CIRCLE('',#5768,0.65);
#1505=CIRCLE('',#5770,0.65);
#1506=CIRCLE('',#5772,0.62);
#1507=CIRCLE('',#5774,0.42);
#1508=CIRCLE('',#5776,0.3933);
#1818=LINE('',#8424,#2228);
#1819=LINE('',#8426,#2229);
#1820=LINE('',#8428,#2230);
#1821=LINE('',#8429,#2231);
#1822=LINE('',#8432,#2232);
#1823=LINE('',#8434,#2233);
#1824=LINE('',#8435,#2234);
#1825=LINE('',#8438,#2235);
#1826=LINE('',#8440,#2236);
#1827=LINE('',#8441,#2237);
#1828=LINE('',#8444,#2238);
#1829=LINE('',#8446,#2239);
#1830=LINE('',#8447,#2240);
#1831=LINE('',#8450,#2241);
#1832=LINE('',#8452,#2242);
#1833=LINE('',#8453,#2243);
#1834=LINE('',#8455,#2244);
#1835=LINE('',#8456,#2245);
#1836=LINE('',#8468,#2246);
#1837=LINE('',#8472,#2247);
#1838=LINE('',#8476,#2248);
#1839=LINE('',#8483,#2249);
#1840=LINE('',#8485,#2250);
#2228=VECTOR('',#6856,1.);
#2229=VECTOR('',#6857,1.);
#2230=VECTOR('',#6858,1.);
#2231=VECTOR('',#6859,1.);
#2232=VECTOR('',#6862,1.);
#2233=VECTOR('',#6863,1.);
#2234=VECTOR('',#6864,1.);
#2235=VECTOR('',#6867,1.);
#2236=VECTOR('',#6868,1.);
#2237=VECTOR('',#6869,1.);
#2238=VECTOR('',#6872,1.);
#2239=VECTOR('',#6873,1.);
#2240=VECTOR('',#6874,1.);
#2241=VECTOR('',#6877,1.);
#2242=VECTOR('',#6878,1.);
#2243=VECTOR('',#6879,1.);
#2244=VECTOR('',#6882,1.);
#2245=VECTOR('',#6883,1.);
#2246=VECTOR('',#6900,0.625);
#2247=VECTOR('',#6905,0.65);
#2248=VECTOR('',#6910,0.635);
#2249=VECTOR('',#6919,0.41);
#2250=VECTOR('',#6922,0.4);
#2650=VERTEX_POINT('',#8422);
#2651=VERTEX_POINT('',#8423);
#2652=VERTEX_POINT('',#8425);
#2653=VERTEX_POINT('',#8427);
#2654=VERTEX_POINT('',#8431);
#2655=VERTEX_POINT('',#8433);
#2656=VERTEX_POINT('',#8437);
#2657=VERTEX_POINT('',#8439);
#2658=VERTEX_POINT('',#8443);
#2659=VERTEX_POINT('',#8445);
#2660=VERTEX_POINT('',#8449);
#2661=VERTEX_POINT('',#8451);
#2662=VERTEX_POINT('',#8460);
#2663=VERTEX_POINT('',#8463);
#2664=VERTEX_POINT('',#8466);
#2665=VERTEX_POINT('',#8470);
#2666=VERTEX_POINT('',#8474);
#2667=VERTEX_POINT('',#8478);
#2668=VERTEX_POINT('',#8481);
#3208=EDGE_CURVE('',#2650,#2651,#1818,.T.);
#3209=EDGE_CURVE('',#2651,#2652,#1819,.T.);
#3210=EDGE_CURVE('',#2652,#2653,#1820,.T.);
#3211=EDGE_CURVE('',#2650,#2653,#1821,.T.);
#3212=EDGE_CURVE('',#2651,#2654,#1822,.T.);
#3213=EDGE_CURVE('',#2654,#2655,#1823,.T.);
#3214=EDGE_CURVE('',#2655,#2652,#1824,.T.);
#3215=EDGE_CURVE('',#2654,#2656,#1825,.T.);
#3216=EDGE_CURVE('',#2656,#2657,#1826,.T.);
#3217=EDGE_CURVE('',#2657,#2655,#1827,.T.);
#3218=EDGE_CURVE('',#2656,#2658,#1828,.T.);
#3219=EDGE_CURVE('',#2658,#2659,#1829,.T.);
#3220=EDGE_CURVE('',#2659,#2657,#1830,.T.);
#3221=EDGE_CURVE('',#2658,#2660,#1831,.T.);
#3222=EDGE_CURVE('',#2660,#2661,#1832,.T.);
#3223=EDGE_CURVE('',#2661,#2659,#1833,.T.);
#3224=EDGE_CURVE('',#2660,#2650,#1834,.T.);
#3225=EDGE_CURVE('',#2653,#2661,#1835,.T.);
#3226=EDGE_CURVE('',#2662,#2662,#1502,.T.);
#3227=EDGE_CURVE('',#2663,#2663,#1503,.T.);
#3228=EDGE_CURVE('',#2664,#2664,#1504,.T.);
#3229=EDGE_CURVE('',#2664,#2663,#1836,.T.);
#3230=EDGE_CURVE('',#2665,#2665,#1505,.T.);
#3231=EDGE_CURVE('',#2665,#2664,#1837,.T.);
#3232=EDGE_CURVE('',#2666,#2666,#1506,.T.);
#3233=EDGE_CURVE('',#2666,#2665,#1838,.T.);
#3234=EDGE_CURVE('',#2667,#2667,#1507,.T.);
#3235=EDGE_CURVE('',#2668,#2668,#1508,.F.);
#3236=EDGE_CURVE('',#2668,#2667,#1839,.T.);
#3237=EDGE_CURVE('',#2662,#2668,#1840,.T.);
#4240=ORIENTED_EDGE('',*,*,#3208,.T.);
#4241=ORIENTED_EDGE('',*,*,#3209,.T.);
#4242=ORIENTED_EDGE('',*,*,#3210,.T.);
#4243=ORIENTED_EDGE('',*,*,#3211,.F.);
#4244=ORIENTED_EDGE('',*,*,#3212,.T.);
#4245=ORIENTED_EDGE('',*,*,#3213,.T.);
#4246=ORIENTED_EDGE('',*,*,#3214,.T.);
#4247=ORIENTED_EDGE('',*,*,#3209,.F.);
#4248=ORIENTED_EDGE('',*,*,#3215,.T.);
#4249=ORIENTED_EDGE('',*,*,#3216,.T.);
#4250=ORIENTED_EDGE('',*,*,#3217,.T.);
#4251=ORIENTED_EDGE('',*,*,#3213,.F.);
#4252=ORIENTED_EDGE('',*,*,#3218,.T.);
#4253=ORIENTED_EDGE('',*,*,#3219,.T.);
#4254=ORIENTED_EDGE('',*,*,#3220,.T.);
#4255=ORIENTED_EDGE('',*,*,#3216,.F.);
#4256=ORIENTED_EDGE('',*,*,#3221,.T.);
#4257=ORIENTED_EDGE('',*,*,#3222,.T.);
#4258=ORIENTED_EDGE('',*,*,#3223,.T.);
#4259=ORIENTED_EDGE('',*,*,#3219,.F.);
#4260=ORIENTED_EDGE('',*,*,#3224,.T.);
#4261=ORIENTED_EDGE('',*,*,#3211,.T.);
#4262=ORIENTED_EDGE('',*,*,#3225,.T.);
#4263=ORIENTED_EDGE('',*,*,#3222,.F.);
#4264=ORIENTED_EDGE('',*,*,#3224,.F.);
#4265=ORIENTED_EDGE('',*,*,#3221,.F.);
#4266=ORIENTED_EDGE('',*,*,#3218,.F.);
#4267=ORIENTED_EDGE('',*,*,#3215,.F.);
#4268=ORIENTED_EDGE('',*,*,#3212,.F.);
#4269=ORIENTED_EDGE('',*,*,#3208,.F.);
#4270=ORIENTED_EDGE('',*,*,#3225,.F.);
#4271=ORIENTED_EDGE('',*,*,#3210,.F.);
#4272=ORIENTED_EDGE('',*,*,#3214,.F.);
#4273=ORIENTED_EDGE('',*,*,#3217,.F.);
#4274=ORIENTED_EDGE('',*,*,#3220,.F.);
#4275=ORIENTED_EDGE('',*,*,#3223,.F.);
#4276=ORIENTED_EDGE('',*,*,#3226,.F.);
#4277=ORIENTED_EDGE('',*,*,#3227,.F.);
#4278=ORIENTED_EDGE('',*,*,#3228,.F.);
#4279=ORIENTED_EDGE('',*,*,#3229,.T.);
#4280=ORIENTED_EDGE('',*,*,#3227,.T.);
#4281=ORIENTED_EDGE('',*,*,#3229,.F.);
#4282=ORIENTED_EDGE('',*,*,#3230,.F.);
#4283=ORIENTED_EDGE('',*,*,#3231,.T.);
#4284=ORIENTED_EDGE('',*,*,#3228,.T.);
#4285=ORIENTED_EDGE('',*,*,#3231,.F.);
#4286=ORIENTED_EDGE('',*,*,#3232,.F.);
#4287=ORIENTED_EDGE('',*,*,#3233,.T.);
#4288=ORIENTED_EDGE('',*,*,#3230,.T.);
#4289=ORIENTED_EDGE('',*,*,#3233,.F.);
#4290=ORIENTED_EDGE('',*,*,#3232,.T.);
#4291=ORIENTED_EDGE('',*,*,#3234,.F.);
#4292=ORIENTED_EDGE('',*,*,#3235,.F.);
#4293=ORIENTED_EDGE('',*,*,#3236,.T.);
#4294=ORIENTED_EDGE('',*,*,#3234,.T.);
#4295=ORIENTED_EDGE('',*,*,#3236,.F.);
#4296=ORIENTED_EDGE('',*,*,#3226,.T.);
#4297=ORIENTED_EDGE('',*,*,#3237,.T.);
#4298=ORIENTED_EDGE('',*,*,#3235,.T.);
#4299=ORIENTED_EDGE('',*,*,#3237,.F.);
#4843=CYLINDRICAL_SURFACE('',#5769,0.65);
#4844=CYLINDRICAL_SURFACE('',#5777,0.3933);
#5035=ADVANCED_FACE('',(#834),#583,.F.);
#5036=ADVANCED_FACE('',(#835),#584,.F.);
#5037=ADVANCED_FACE('',(#836),#585,.F.);
#5038=ADVANCED_FACE('',(#837),#586,.F.);
#5039=ADVANCED_FACE('',(#838),#587,.F.);
#5040=ADVANCED_FACE('',(#839),#588,.F.);
#5041=ADVANCED_FACE('',(#840),#589,.F.);
#5042=ADVANCED_FACE('',(#841),#590,.F.);
#5043=ADVANCED_FACE('',(#842),#591,.F.);
#5044=ADVANCED_FACE('',(#843),#592,.T.);
#5045=ADVANCED_FACE('',(#844),#261,.T.);
#5046=ADVANCED_FACE('',(#845),#4843,.T.);
#5047=ADVANCED_FACE('',(#846),#262,.T.);
#5048=ADVANCED_FACE('',(#847,#452),#593,.T.);
#5049=ADVANCED_FACE('',(#848),#263,.T.);
#5050=ADVANCED_FACE('',(#849),#4844,.T.);
#5181=CLOSED_SHELL('',(#5035,#5036,#5037,#5038,#5039,#5040,#5041,#5042));
#5182=CLOSED_SHELL('',(#5043,#5044,#5045,#5046,#5047,#5048,#5049,#5050));
#5754=AXIS2_PLACEMENT_3D('',#8420,#6852,#6853);
#5755=AXIS2_PLACEMENT_3D('',#8421,#6854,#6855);
#5756=AXIS2_PLACEMENT_3D('',#8430,#6860,#6861);
#5757=AXIS2_PLACEMENT_3D('',#8436,#6865,#6866);
#5758=AXIS2_PLACEMENT_3D('',#8442,#6870,#6871);
#5759=AXIS2_PLACEMENT_3D('',#8448,#6875,#6876);
#5760=AXIS2_PLACEMENT_3D('',#8454,#6880,#6881);
#5761=AXIS2_PLACEMENT_3D('',#8457,#6884,#6885);
#5762=AXIS2_PLACEMENT_3D('',#8458,#6886,#6887);
#5763=AXIS2_PLACEMENT_3D('',#8459,#6888,#6889);
#5764=AXIS2_PLACEMENT_3D('',#8461,#6890,#6891);
#5765=AXIS2_PLACEMENT_3D('',#8462,#6892,#6893);
#5766=AXIS2_PLACEMENT_3D('',#8464,#6894,#6895);
#5767=AXIS2_PLACEMENT_3D('',#8465,#6896,#6897);
#5768=AXIS2_PLACEMENT_3D('',#8467,#6898,#6899);
#5769=AXIS2_PLACEMENT_3D('',#8469,#6901,#6902);
#5770=AXIS2_PLACEMENT_3D('',#8471,#6903,#6904);
#5771=AXIS2_PLACEMENT_3D('',#8473,#6906,#6907);
#5772=AXIS2_PLACEMENT_3D('',#8475,#6908,#6909);
#5773=AXIS2_PLACEMENT_3D('',#8477,#6911,#6912);
#5774=AXIS2_PLACEMENT_3D('',#8479,#6913,#6914);
#5775=AXIS2_PLACEMENT_3D('',#8480,#6915,#6916);
#5776=AXIS2_PLACEMENT_3D('',#8482,#6917,#6918);
#5777=AXIS2_PLACEMENT_3D('',#8484,#6920,#6921);
#6852=DIRECTION('axis',(0.,0.,1.));
#6853=DIRECTION('refdir',(1.,0.,0.));
#6854=DIRECTION('center_axis',(0.866025403784439,0.,-0.5));
#6855=DIRECTION('ref_axis',(0.5,0.,0.866025403784439));
#6856=DIRECTION('',(-0.5,0.,-0.866025403784439));
#6857=DIRECTION('',(0.,-1.,0.));
#6858=DIRECTION('',(0.5,0.,0.866025403784439));
#6859=DIRECTION('',(0.,-1.,0.));
#6860=DIRECTION('center_axis',(1.60246890531964E-16,0.,-1.));
#6861=DIRECTION('ref_axis',(1.,0.,1.60246890531964E-16));
#6862=DIRECTION('',(-1.,0.,-1.60246890531964E-16));
#6863=DIRECTION('',(0.,-1.,0.));
#6864=DIRECTION('',(1.,0.,1.60246890531964E-16));
#6865=DIRECTION('center_axis',(-0.866025403784439,0.,-0.5));
#6866=DIRECTION('ref_axis',(0.5,0.,-0.866025403784439));
#6867=DIRECTION('',(-0.5,0.,0.866025403784439));
#6868=DIRECTION('',(0.,-1.,0.));
#6869=DIRECTION('',(0.5,0.,-0.866025403784439));
#6870=DIRECTION('center_axis',(-0.866025403784439,0.,0.5));
#6871=DIRECTION('ref_axis',(-0.5,0.,-0.866025403784439));
#6872=DIRECTION('',(0.5,0.,0.866025403784439));
#6873=DIRECTION('',(0.,-1.,0.));
#6874=DIRECTION('',(-0.5,0.,-0.866025403784439));
#6875=DIRECTION('center_axis',(-1.60246890531964E-16,0.,1.));
#6876=DIRECTION('ref_axis',(-1.,0.,-1.60246890531964E-16));
#6877=DIRECTION('',(1.,0.,1.60246890531964E-16));
#6878=DIRECTION('',(0.,-1.,0.));
#6879=DIRECTION('',(-1.,0.,-1.60246890531964E-16));
#6880=DIRECTION('center_axis',(0.866025403784439,0.,0.5));
#6881=DIRECTION('ref_axis',(-0.5,0.,0.866025403784439));
#6882=DIRECTION('',(0.5,0.,-0.866025403784439));
#6883=DIRECTION('',(-0.5,0.,0.866025403784439));
#6884=DIRECTION('center_axis',(0.,1.,0.));
#6885=DIRECTION('ref_axis',(1.,0.,0.));
#6886=DIRECTION('center_axis',(0.,-1.,0.));
#6887=DIRECTION('ref_axis',(0.,0.,-1.));
#6888=DIRECTION('center_axis',(0.,1.,0.));
#6889=DIRECTION('ref_axis',(1.,0.,0.));
#6890=DIRECTION('center_axis',(0.,1.,0.));
#6891=DIRECTION('ref_axis',(1.,0.,0.));
#6892=DIRECTION('center_axis',(0.,1.,0.));
#6893=DIRECTION('ref_axis',(0.,0.,1.));
#6894=DIRECTION('center_axis',(0.,-1.,0.));
#6895=DIRECTION('ref_axis',(1.,0.,0.));
#6896=DIRECTION('center_axis',(0.,-1.,0.));
#6897=DIRECTION('ref_axis',(1.,0.,0.));
#6898=DIRECTION('center_axis',(0.,-1.,0.));
#6899=DIRECTION('ref_axis',(1.,0.,0.));
#6900=DIRECTION('',(0.707106781186548,0.707106781186547,8.65956056235493E-17));
#6901=DIRECTION('center_axis',(0.,-1.,0.));
#6902=DIRECTION('ref_axis',(1.,0.,0.));
#6903=DIRECTION('center_axis',(0.,-1.,0.));
#6904=DIRECTION('ref_axis',(1.,0.,0.));
#6905=DIRECTION('',(0.,1.,0.));
#6906=DIRECTION('center_axis',(0.,1.,0.));
#6907=DIRECTION('ref_axis',(1.,0.,0.));
#6908=DIRECTION('center_axis',(0.,-1.,0.));
#6909=DIRECTION('ref_axis',(1.,0.,0.));
#6910=DIRECTION('',(-0.707106781186548,0.707106781186547,-8.65956056235494E-17));
#6911=DIRECTION('center_axis',(0.,-1.,0.));
#6912=DIRECTION('ref_axis',(0.,0.,-1.));
#6913=DIRECTION('center_axis',(0.,-1.,0.));
#6914=DIRECTION('ref_axis',(1.,0.,0.));
#6915=DIRECTION('center_axis',(0.,1.,0.));
#6916=DIRECTION('ref_axis',(1.,0.,0.));
#6917=DIRECTION('center_axis',(0.,1.,0.));
#6918=DIRECTION('ref_axis',(1.,0.,0.));
#6919=DIRECTION('',(-0.447213595499958,0.894427190999916,-5.47678698264203E-17));
#6920=DIRECTION('center_axis',(0.,-1.,0.));
#6921=DIRECTION('ref_axis',(1.,0.,0.));
#6922=DIRECTION('',(0.,1.,0.));
#8420=CARTESIAN_POINT('',(0.,0.,0.));
#8421=CARTESIAN_POINT('Origin',(0.173205080756888,-0.8,-0.3));
#8422=CARTESIAN_POINT('',(0.346410161513775,-0.8,0.));
#8423=CARTESIAN_POINT('',(0.173205080756888,-0.8,-0.3));
#8424=CARTESIAN_POINT('',(0.346410161513775,-0.8,0.));
#8425=CARTESIAN_POINT('',(0.173205080756888,-1.28,-0.3));
#8426=CARTESIAN_POINT('',(0.173205080756888,-0.8,-0.3));
#8427=CARTESIAN_POINT('',(0.346410161513775,-1.28,0.));
#8428=CARTESIAN_POINT('',(0.346410161513775,-1.28,0.));
#8429=CARTESIAN_POINT('',(0.346410161513775,-0.8,0.));
#8430=CARTESIAN_POINT('Origin',(-0.173205080756888,-0.8,-0.3));
#8431=CARTESIAN_POINT('',(-0.173205080756888,-0.8,-0.3));
#8432=CARTESIAN_POINT('',(0.173205080756888,-0.8,-0.3));
#8433=CARTESIAN_POINT('',(-0.173205080756888,-1.28,-0.3));
#8434=CARTESIAN_POINT('',(-0.173205080756888,-0.8,-0.3));
#8435=CARTESIAN_POINT('',(0.173205080756888,-1.28,-0.3));
#8436=CARTESIAN_POINT('Origin',(-0.346410161513775,-0.8,-5.55111512312578E-17));
#8437=CARTESIAN_POINT('',(-0.346410161513775,-0.8,-4.24230095489963E-17));
#8438=CARTESIAN_POINT('',(-0.173205080756888,-0.8,-0.3));
#8439=CARTESIAN_POINT('',(-0.346410161513775,-1.28,-5.55111512312578E-17));
#8440=CARTESIAN_POINT('',(-0.346410161513775,-0.8,-4.24230095489963E-17));
#8441=CARTESIAN_POINT('',(-0.173205080756888,-1.28,-0.3));
#8442=CARTESIAN_POINT('Origin',(-0.173205080756888,-0.8,0.3));
#8443=CARTESIAN_POINT('',(-0.173205080756888,-0.8,0.3));
#8444=CARTESIAN_POINT('',(-0.346410161513775,-0.8,-4.24230095489963E-17));
#8445=CARTESIAN_POINT('',(-0.173205080756888,-1.28,0.3));
#8446=CARTESIAN_POINT('',(-0.173205080756888,-0.8,0.3));
#8447=CARTESIAN_POINT('',(-0.346410161513775,-1.28,-4.24230095489963E-17));
#8448=CARTESIAN_POINT('Origin',(0.173205080756888,-0.8,0.3));
#8449=CARTESIAN_POINT('',(0.173205080756888,-0.8,0.3));
#8450=CARTESIAN_POINT('',(-0.173205080756888,-0.8,0.3));
#8451=CARTESIAN_POINT('',(0.173205080756888,-1.28,0.3));
#8452=CARTESIAN_POINT('',(0.173205080756888,-0.8,0.3));
#8453=CARTESIAN_POINT('',(-0.173205080756888,-1.28,0.3));
#8454=CARTESIAN_POINT('Origin',(0.346410161513775,-0.8,0.));
#8455=CARTESIAN_POINT('',(0.173205080756888,-0.8,0.3));
#8456=CARTESIAN_POINT('',(0.173205080756888,-1.28,0.3));
#8457=CARTESIAN_POINT('Origin',(0.,-0.8,-5.55111512312578E-17));
#8458=CARTESIAN_POINT('Origin',(0.,-1.28,-5.55111512312578E-17));
#8459=CARTESIAN_POINT('Origin',(0.,-2.5,0.));
#8460=CARTESIAN_POINT('',(-0.3933,-2.5,4.81653586104654E-17));
#8461=CARTESIAN_POINT('Origin',(0.,-2.5,0.));
#8462=CARTESIAN_POINT('Origin',(0.6,0.8,0.));
#8463=CARTESIAN_POINT('',(-0.6,0.8,-7.34788079488412E-17));
#8464=CARTESIAN_POINT('Origin',(0.,0.8,0.));
#8465=CARTESIAN_POINT('Origin',(0.,0.775,0.));
#8466=CARTESIAN_POINT('',(-0.65,0.75,-7.9602041944578E-17));
#8467=CARTESIAN_POINT('Origin',(0.,0.75,0.));
#8468=CARTESIAN_POINT('',(-0.625,0.775,-7.65404249467096E-17));
#8469=CARTESIAN_POINT('Origin',(0.,0.39,0.));
#8470=CARTESIAN_POINT('',(-0.65,0.0299999999999998,-7.9602041944578E-17));
#8471=CARTESIAN_POINT('Origin',(0.,0.0299999999999998,0.));
#8472=CARTESIAN_POINT('',(-0.65,0.39,-7.9602041944578E-17));
#8473=CARTESIAN_POINT('Origin',(0.,0.0150000000000001,0.));
#8474=CARTESIAN_POINT('',(-0.62,5.89805981832114E-17,-7.59281015471359E-17));
#8475=CARTESIAN_POINT('Origin',(0.,0.,0.));
#8476=CARTESIAN_POINT('',(-0.635,0.0150000000000001,-7.77650717458569E-17));
#8477=CARTESIAN_POINT('Origin',(0.42,0.,0.));
#8478=CARTESIAN_POINT('',(-0.42,-3.46944695195361E-18,-5.14351655641888E-17));
#8479=CARTESIAN_POINT('Origin',(0.,0.,0.));
#8480=CARTESIAN_POINT('Origin',(0.,-0.02,0.));
#8481=CARTESIAN_POINT('',(-0.3933,-0.0534000000000001,4.81653586104654E-17));
#8482=CARTESIAN_POINT('Origin',(0.,-0.0534000000000001,0.));
#8483=CARTESIAN_POINT('',(-0.41,-0.02,-5.02105187650415E-17));
#8484=CARTESIAN_POINT('Origin',(0.,-1.48,0.));
#8485=CARTESIAN_POINT('',(-0.3933,-1.48,-4.81653586104654E-17));
#9239=UNCERTAINTY_MEASURE_WITH_UNIT(LENGTH_MEASURE(0.001),#9286,
'DISTANCE_ACCURACY_VALUE',
'Maximum model space distance between geometric entities at asserted c
onnectivities');
#9255=UNCERTAINTY_MEASURE_WITH_UNIT(LENGTH_MEASURE(0.001),#9286,
'DISTANCE_ACCURACY_VALUE',
'Maximum model space distance between geometric entities at asserted c
onnectivities');
#9269=(
GEOMETRIC_REPRESENTATION_CONTEXT(3)
GLOBAL_UNCERTAINTY_ASSIGNED_CONTEXT((#9239))
GLOBAL_UNIT_ASSIGNED_CONTEXT((#9286,#9288,#9289))
REPRESENTATION_CONTEXT('','3D')
);
#9285=(
GEOMETRIC_REPRESENTATION_CONTEXT(3)
GLOBAL_UNCERTAINTY_ASSIGNED_CONTEXT((#9255))
GLOBAL_UNIT_ASSIGNED_CONTEXT((#9286,#9288,#9289))
REPRESENTATION_CONTEXT('','3D')
);
#9286=(
LENGTH_UNIT()
NAMED_UNIT(*)
SI_UNIT(.CENTI.,.METRE.)
);
#9288=(
NAMED_UNIT(*)
PLANE_ANGLE_UNIT()
SI_UNIT($,.RADIAN.)
);
#9289=(
NAMED_UNIT(*)
SI_UNIT($,.STERADIAN.)
SOLID_ANGLE_UNIT()
);
#9303=SHAPE_DEFINITION_REPRESENTATION(#9332,#9407);
#9332=PRODUCT_DEFINITION_SHAPE('',$,#9437);
#9407=SHAPE_REPRESENTATION('',(#5754),#9269);
#9423=PRODUCT_DEFINITION_CONTEXT('part definition',#9512,'design');
#9437=PRODUCT_DEFINITION('M8x25 Bolt','M8x25 Bolt',#9466,#9423);
#9466=PRODUCT_DEFINITION_FORMATION('',$,#9527);
#9512=APPLICATION_CONTEXT(
'Core Data for Automotive Mechanical Design Process');
#9513=PRODUCT_CONTEXT('part definition',#9512,'mechanical');
#9527=PRODUCT('M8x25 Bolt','M8x25 Bolt','M8x25 Bolt',(#9513));
#9613=COLOUR_RGB('Black',0.12,0.14,0.17);
#9614=FILL_AREA_STYLE_COLOUR('',#9613);
#9615=FILL_AREA_STYLE('',(#9614));
#9616=SURFACE_STYLE_FILL_AREA(#9615);
#9617=SURFACE_SIDE_STYLE('',(#9616));
#9618=SURFACE_STYLE_USAGE(.BOTH.,#9617);
#9619=PRESENTATION_STYLE_ASSIGNMENT((#9618));
ENDSEC;
END-ISO-10303-21;
